ISO-10303-21;
HEADER;
/* Generated by software containing ST-Developer
 * from STEP Tools, Inc. (www.steptools.com) 
 */

FILE_DESCRIPTION(
/* description */ ('PAT-072'),
/* implementation_level */ '2;1');

FILE_NAME(
/* name */ 'Metering stem gasket (1).step',
/* time_stamp */ '2026-10-29T20:11:56-07:00',
/* author */ (''),
/* organization */ (''),
/* preprocessor_version */ 'ST-DEVELOPER v20.2',
/* originating_system */ 'Autodesk Translation Framework v15.17.0.0',
/* authorisation */ '');

FILE_SCHEMA (('AUTOMOTIVE_DESIGN { 1 0 10303 214 3 1 1 }'));
ENDSEC;

DATA;
#10=MECHANICAL_DESIGN_GEOMETRIC_PRESENTATION_REPRESENTATION('',(#341),#11432);
#269=SHAPE_REPRESENTATION_RELATIONSHIP('SRR','None',#11573,#305);
#305=ADVANCED_BREP_SHAPE_REPRESENTATION('',(#377),#11404);
#341=STYLED_ITEM('',(#11833),#377);
#377=MANIFOLD_SOLID_BREP('Body1',#6076);
#470=FACE_BOUND('',#1362,.T.);
#471=FACE_BOUND('',#1364,.T.);
#635=PLANE('',#6754);
#636=PLANE('',#6755);
#919=FACE_OUTER_BOUND('',#1359,.T.);
#920=FACE_OUTER_BOUND('',#1360,.T.);
#921=FACE_OUTER_BOUND('',#1361,.T.);
#922=FACE_OUTER_BOUND('',#1363,.T.);
#1359=EDGE_LOOP('',(#4570,#4571,#4572,#4573));
#1360=EDGE_LOOP('',(#4574,#4575,#4576,#4577));
#1361=EDGE_LOOP('',(#4578));
#1362=EDGE_LOOP('',(#4579));
#1363=EDGE_LOOP('',(#4580));
#1364=EDGE_LOOP('',(#4581));
#1822=LINE('',#10084,#2241);
#1823=LINE('',#10090,#2242);
#2241=VECTOR('',#7869,0.3);
#2242=VECTOR('',#7876,0.5);
#2651=CIRCLE('',#6749,0.3);
#2652=CIRCLE('',#6750,0.3);
#2653=CIRCLE('',#6752,0.5);
#2654=CIRCLE('',#6753,0.5);
#3000=VERTEX_POINT('',#10081);
#3001=VERTEX_POINT('',#10083);
#3002=VERTEX_POINT('',#10087);
#3003=VERTEX_POINT('',#10089);
#3574=EDGE_CURVE('',#3000,#3000,#2651,.T.);
#3575=EDGE_CURVE('',#3000,#3001,#1822,.T.);
#3576=EDGE_CURVE('',#3001,#3001,#2652,.T.);
#3577=EDGE_CURVE('',#3002,#3002,#2653,.T.);
#3578=EDGE_CURVE('',#3002,#3003,#1823,.T.);
#3579=EDGE_CURVE('',#3003,#3003,#2654,.T.);
#4570=ORIENTED_EDGE('',*,*,#3574,.F.);
#4571=ORIENTED_EDGE('',*,*,#3575,.T.);
#4572=ORIENTED_EDGE('',*,*,#3576,.T.);
#4573=ORIENTED_EDGE('',*,*,#3575,.F.);
#4574=ORIENTED_EDGE('',*,*,#3577,.F.);
#4575=ORIENTED_EDGE('',*,*,#3578,.T.);
#4576=ORIENTED_EDGE('',*,*,#3579,.T.);
#4577=ORIENTED_EDGE('',*,*,#3578,.F.);
#4578=ORIENTED_EDGE('',*,*,#3577,.T.);
#4579=ORIENTED_EDGE('',*,*,#3574,.T.);
#4580=ORIENTED_EDGE('',*,*,#3579,.F.);
#4581=ORIENTED_EDGE('',*,*,#3576,.F.);
#5616=CYLINDRICAL_SURFACE('',#6748,0.3);
#5617=CYLINDRICAL_SURFACE('',#6751,0.5);
#5818=ADVANCED_FACE('',(#919),#5616,.F.);
#5819=ADVANCED_FACE('',(#920),#5617,.T.);
#5820=ADVANCED_FACE('',(#921,#470),#635,.T.);
#5821=ADVANCED_FACE('',(#922,#471),#636,.F.);
#6076=CLOSED_SHELL('',(#5818,#5819,#5820,#5821));
#6747=AXIS2_PLACEMENT_3D('',#10079,#7863,#7864);
#6748=AXIS2_PLACEMENT_3D('',#10080,#7865,#7866);
#6749=AXIS2_PLACEMENT_3D('',#10082,#7867,#7868);
#6750=AXIS2_PLACEMENT_3D('',#10085,#7870,#7871);
#6751=AXIS2_PLACEMENT_3D('',#10086,#7872,#7873);
#6752=AXIS2_PLACEMENT_3D('',#10088,#7874,#7875);
#6753=AXIS2_PLACEMENT_3D('',#10091,#7877,#7878);
#6754=AXIS2_PLACEMENT_3D('',#10092,#7879,#7880);
#6755=AXIS2_PLACEMENT_3D('',#10093,#7881,#7882);
#7863=DIRECTION('axis',(0.,0.,1.));
#7864=DIRECTION('refdir',(1.,0.,0.));
#7865=DIRECTION('center_axis',(0.,0.,1.));
#7866=DIRECTION('ref_axis',(1.,0.,0.));
#7867=DIRECTION('center_axis',(0.,0.,-1.));
#7868=DIRECTION('ref_axis',(1.,0.,0.));
#7869=DIRECTION('',(0.,0.,-1.));
#7870=DIRECTION('center_axis',(0.,0.,-1.));
#7871=DIRECTION('ref_axis',(1.,0.,0.));
#7872=DIRECTION('center_axis',(0.,0.,1.));
#7873=DIRECTION('ref_axis',(1.,0.,0.));
#7874=DIRECTION('center_axis',(0.,0.,1.));
#7875=DIRECTION('ref_axis',(1.,0.,0.));
#7876=DIRECTION('',(0.,0.,-1.));
#7877=DIRECTION('center_axis',(0.,0.,1.));
#7878=DIRECTION('ref_axis',(1.,0.,0.));
#7879=DIRECTION('center_axis',(0.,0.,1.));
#7880=DIRECTION('ref_axis',(1.,0.,0.));
#7881=DIRECTION('center_axis',(0.,0.,1.));
#7882=DIRECTION('ref_axis',(1.,0.,0.));
#10079=CARTESIAN_POINT('',(0.,0.,0.));
#10080=CARTESIAN_POINT('Origin',(-1.25,1.5,6.));
#10081=CARTESIAN_POINT('',(-1.55,1.5,6.1));
#10082=CARTESIAN_POINT('Origin',(-1.25,1.5,6.1));
#10083=CARTESIAN_POINT('',(-1.55,1.5,6.));
#10084=CARTESIAN_POINT('',(-1.55,1.5,6.));
#10085=CARTESIAN_POINT('Origin',(-1.25,1.5,6.));
#10086=CARTESIAN_POINT('Origin',(-1.25,1.5,6.));
#10087=CARTESIAN_POINT('',(-1.75,1.5,6.1));
#10088=CARTESIAN_POINT('Origin',(-1.25,1.5,6.1));
#10089=CARTESIAN_POINT('',(-1.75,1.5,6.));
#10090=CARTESIAN_POINT('',(-1.75,1.5,6.));
#10091=CARTESIAN_POINT('Origin',(-1.25,1.5,6.));
#10092=CARTESIAN_POINT('Origin',(-1.25,1.5,6.1));
#10093=CARTESIAN_POINT('Origin',(-1.25,1.5,6.));
#11365=UNCERTAINTY_MEASURE_WITH_UNIT(LENGTH_MEASURE(0.001),#11433,
'DISTANCE_ACCURACY_VALUE',
'Maximum model space distance between geometric entities at asserted c
onnectivities');
#11393=UNCERTAINTY_MEASURE_WITH_UNIT(LENGTH_MEASURE(0.001),#11433,
'DISTANCE_ACCURACY_VALUE',
'Maximum model space distance between geometric entities at asserted c
onnectivities');
#11404=(
GEOMETRIC_REPRESENTATION_CONTEXT(3)
GLOBAL_UNCERTAINTY_ASSIGNED_CONTEXT((#11365))
GLOBAL_UNIT_ASSIGNED_CONTEXT((#11433,#11435,#11436))
REPRESENTATION_CONTEXT('','3D')
);
#11432=(
GEOMETRIC_REPRESENTATION_CONTEXT(3)
GLOBAL_UNCERTAINTY_ASSIGNED_CONTEXT((#11393))
GLOBAL_UNIT_ASSIGNED_CONTEXT((#11433,#11435,#11436))
REPRESENTATION_CONTEXT('','3D')
);
#11433=(
LENGTH_UNIT()
NAMED_UNIT(*)
SI_UNIT(.CENTI.,.METRE.)
);
#11435=(
NAMED_UNIT(*)
PLANE_ANGLE_UNIT()
SI_UNIT($,.RADIAN.)
);
#11436=(
NAMED_UNIT(*)
SI_UNIT($,.STERADIAN.)
SOLID_ANGLE_UNIT()
);
#11447=SHAPE_DEFINITION_REPRESENTATION(#11485,#11573);
#11485=PRODUCT_DEFINITION_SHAPE('',$,#11612);
#11573=SHAPE_REPRESENTATION('',(#6747),#11404);
#11601=PRODUCT_DEFINITION_CONTEXT('part definition',#11717,'design');
#11612=PRODUCT_DEFINITION('Metering stem gasket (1)',
'Metering stem gasket (1)',#11650,#11601);
#11650=PRODUCT_DEFINITION_FORMATION('',$,#11729);
#11717=APPLICATION_CONTEXT(
'Core Data for Automotive Mechanical Design Process');
#11718=PRODUCT_CONTEXT('part definition',#11717,'mechanical');
#11729=PRODUCT('Metering stem gasket (1)','Metering stem gasket (1)',
'Metering stem gasket (1)',(#11718));
#11827=COLOUR_RGB('Off White',0.89,0.88,0.83);
#11828=FILL_AREA_STYLE_COLOUR('',#11827);
#11829=FILL_AREA_STYLE('',(#11828));
#11830=SURFACE_STYLE_FILL_AREA(#11829);
#11831=SURFACE_SIDE_STYLE('',(#11830));
#11832=SURFACE_STYLE_USAGE(.BOTH.,#11831);
#11833=PRESENTATION_STYLE_ASSIGNMENT((#11832));
ENDSEC;
END-ISO-10303-21;
